ISO-10303-21;
HEADER;
/* Generated by software containing ST-Developer
 * from STEP Tools, Inc. (www.steptools.com) 
 */

FILE_DESCRIPTION(
/* description */ ('STEP AP214'),
/* implementation_level */ '2;1');

FILE_NAME(
/* name */ 'High Strength Hex Nut DIN 6915 M16.step',
/* time_stamp */ '2026-11-14T07:13:32-08:00',
/* author */ (''),
/* organization */ (''),
/* preprocessor_version */ 'ST-DEVELOPER v20.2',
/* originating_system */ 'Autodesk Translation Framework v15.17.0.0',
/* authorisation */ '');

FILE_SCHEMA (('AUTOMOTIVE_DESIGN { 1 0 10303 214 3 1 1 }'));
ENDSEC;

DATA;
#10=MECHANICAL_DESIGN_GEOMETRIC_PRESENTATION_REPRESENTATION('',(#1379),#32903);
#550=(
BOUNDED_CURVE()
B_SPLINE_CURVE(2,(#32689,#32690,#32691),.UNSPECIFIED.,.F.,.F.)
B_SPLINE_CURVE_WITH_KNOTS((3,3),(2.31550755136326,3.79303994872323),
 .UNSPECIFIED.)
CURVE()
GEOMETRIC_REPRESENTATION_ITEM()
RATIONAL_B_SPLINE_CURVE((1.76182294006033,1.89810041873942,1.89810041873942))
REPRESENTATION_ITEM('')
);
#551=(
BOUNDED_CURVE()
B_SPLINE_CURVE(2,(#32693,#32694,#32695),.UNSPECIFIED.,.F.,.F.)
B_SPLINE_CURVE_WITH_KNOTS((3,3),(3.79303994872323,5.27057234608321),
 .UNSPECIFIED.)
CURVE()
GEOMETRIC_REPRESENTATION_ITEM()
RATIONAL_B_SPLINE_CURVE((1.89810041873942,1.89810041873942,1.76182294006033))
REPRESENTATION_ITEM('')
);
#552=(
BOUNDED_CURVE()
B_SPLINE_CURVE(2,(#32699,#32700,#32701),.UNSPECIFIED.,.F.,.F.)
B_SPLINE_CURVE_WITH_KNOTS((3,3),(-3.79303994872324,-2.31550755136325),
 .UNSPECIFIED.)
CURVE()
GEOMETRIC_REPRESENTATION_ITEM()
RATIONAL_B_SPLINE_CURVE((1.89810041873942,1.89810041873942,1.76182294006033))
REPRESENTATION_ITEM('')
);
#553=(
BOUNDED_CURVE()
B_SPLINE_CURVE(2,(#32702,#32703,#32704),.UNSPECIFIED.,.F.,.F.)
B_SPLINE_CURVE_WITH_KNOTS((3,3),(-5.27057234608319,-3.79303994872324),
 .UNSPECIFIED.)
CURVE()
GEOMETRIC_REPRESENTATION_ITEM()
RATIONAL_B_SPLINE_CURVE((1.76182294006033,1.89810041873942,1.89810041873942))
REPRESENTATION_ITEM('')
);
#554=(
BOUNDED_CURVE()
B_SPLINE_CURVE(2,(#32707,#32708,#32709),.UNSPECIFIED.,.F.,.F.)
B_SPLINE_CURVE_WITH_KNOTS((3,3),(2.31550755136325,3.79303994872323),
 .UNSPECIFIED.)
CURVE()
GEOMETRIC_REPRESENTATION_ITEM()
RATIONAL_B_SPLINE_CURVE((1.76182294006033,1.89810041873942,1.89810041873942))
REPRESENTATION_ITEM('')
);
#555=(
BOUNDED_CURVE()
B_SPLINE_CURVE(2,(#32711,#32712,#32713),.UNSPECIFIED.,.F.,.F.)
B_SPLINE_CURVE_WITH_KNOTS((3,3),(3.79303994872323,5.27057234608319),
 .UNSPECIFIED.)
CURVE()
GEOMETRIC_REPRESENTATION_ITEM()
RATIONAL_B_SPLINE_CURVE((1.89810041873942,1.89810041873941,1.76182294006033))
REPRESENTATION_ITEM('')
);
#556=(
BOUNDED_CURVE()
B_SPLINE_CURVE(2,(#32717,#32718,#32719),.UNSPECIFIED.,.F.,.F.)
B_SPLINE_CURVE_WITH_KNOTS((3,3),(-3.79303994872322,-2.31550755136326),
 .UNSPECIFIED.)
CURVE()
GEOMETRIC_REPRESENTATION_ITEM()
RATIONAL_B_SPLINE_CURVE((1.89810041873942,1.89810041873942,1.76182294006033))
REPRESENTATION_ITEM('')
);
#557=(
BOUNDED_CURVE()
B_SPLINE_CURVE(2,(#32720,#32721,#32722),.UNSPECIFIED.,.F.,.F.)
B_SPLINE_CURVE_WITH_KNOTS((3,3),(-5.27057234608319,-3.79303994872322),
 .UNSPECIFIED.)
CURVE()
GEOMETRIC_REPRESENTATION_ITEM()
RATIONAL_B_SPLINE_CURVE((1.76182294006033,1.89810041873942,1.89810041873942))
REPRESENTATION_ITEM('')
);
#558=(
BOUNDED_CURVE()
B_SPLINE_CURVE(2,(#32726,#32727,#32728),.UNSPECIFIED.,.F.,.F.)
B_SPLINE_CURVE_WITH_KNOTS((3,3),(2.31550755136325,3.79303994872322),
 .UNSPECIFIED.)
CURVE()
GEOMETRIC_REPRESENTATION_ITEM()
RATIONAL_B_SPLINE_CURVE((1.76182294006033,1.89810041873941,1.89810041873941))
REPRESENTATION_ITEM('')
);
#559=(
BOUNDED_CURVE()
B_SPLINE_CURVE(2,(#32732,#32733,#32734),.UNSPECIFIED.,.F.,.F.)
B_SPLINE_CURVE_WITH_KNOTS((3,3),(-5.27057234608321,-3.79303994872322),
 .UNSPECIFIED.)
CURVE()
GEOMETRIC_REPRESENTATION_ITEM()
RATIONAL_B_SPLINE_CURVE((1.76182294006033,1.89810041873941,1.89810041873941))
REPRESENTATION_ITEM('')
);
#560=(
BOUNDED_CURVE()
B_SPLINE_CURVE(2,(#32735,#32736,#32737),.UNSPECIFIED.,.F.,.F.)
B_SPLINE_CURVE_WITH_KNOTS((3,3),(-3.79303994872322,-2.31550755136325),
 .UNSPECIFIED.)
CURVE()
GEOMETRIC_REPRESENTATION_ITEM()
RATIONAL_B_SPLINE_CURVE((1.89810041873941,1.89810041873941,1.76182294006033))
REPRESENTATION_ITEM('')
);
#561=(
BOUNDED_CURVE()
B_SPLINE_CURVE(2,(#32738,#32739,#32740),.UNSPECIFIED.,.F.,.F.)
B_SPLINE_CURVE_WITH_KNOTS((3,3),(3.79303994872322,5.2705723460832),
 .UNSPECIFIED.)
CURVE()
GEOMETRIC_REPRESENTATION_ITEM()
RATIONAL_B_SPLINE_CURVE((1.89810041873941,1.89810041873941,1.76182294006033))
REPRESENTATION_ITEM('')
);
#562=(
BOUNDED_CURVE()
B_SPLINE_CURVE(2,(#32743,#32744,#32745),.UNSPECIFIED.,.F.,.F.)
B_SPLINE_CURVE_WITH_KNOTS((3,3),(2.31550755136326,3.79303994872322),
 .UNSPECIFIED.)
CURVE()
GEOMETRIC_REPRESENTATION_ITEM()
RATIONAL_B_SPLINE_CURVE((1.76182294006033,1.89810041873941,1.89810041873941))
REPRESENTATION_ITEM('')
);
#563=(
BOUNDED_CURVE()
B_SPLINE_CURVE(2,(#32747,#32748,#32749),.UNSPECIFIED.,.F.,.F.)
B_SPLINE_CURVE_WITH_KNOTS((3,3),(3.79303994872322,5.2705723460832),
 .UNSPECIFIED.)
CURVE()
GEOMETRIC_REPRESENTATION_ITEM()
RATIONAL_B_SPLINE_CURVE((1.89810041873941,1.89810041873941,1.76182294006033))
REPRESENTATION_ITEM('')
);
#564=(
BOUNDED_CURVE()
B_SPLINE_CURVE(2,(#32753,#32754,#32755),.UNSPECIFIED.,.F.,.F.)
B_SPLINE_CURVE_WITH_KNOTS((3,3),(-3.79303994872323,-2.31550755136325),
 .UNSPECIFIED.)
CURVE()
GEOMETRIC_REPRESENTATION_ITEM()
RATIONAL_B_SPLINE_CURVE((1.89810041873941,1.89810041873941,1.76182294006033))
REPRESENTATION_ITEM('')
);
#565=(
BOUNDED_CURVE()
B_SPLINE_CURVE(2,(#32756,#32757,#32758),.UNSPECIFIED.,.F.,.F.)
B_SPLINE_CURVE_WITH_KNOTS((3,3),(-5.27057234608319,-3.79303994872323),
 .UNSPECIFIED.)
CURVE()
GEOMETRIC_REPRESENTATION_ITEM()
RATIONAL_B_SPLINE_CURVE((1.76182294006033,1.89810041873941,1.89810041873941))
REPRESENTATION_ITEM('')
);
#566=(
BOUNDED_CURVE()
B_SPLINE_CURVE(2,(#32761,#32762,#32763),.UNSPECIFIED.,.F.,.F.)
B_SPLINE_CURVE_WITH_KNOTS((3,3),(2.31550755136326,3.79303994872322),
 .UNSPECIFIED.)
CURVE()
GEOMETRIC_REPRESENTATION_ITEM()
RATIONAL_B_SPLINE_CURVE((1.76182294006033,1.89810041873941,1.89810041873941))
REPRESENTATION_ITEM('')
);
#567=(
BOUNDED_CURVE()
B_SPLINE_CURVE(2,(#32765,#32766,#32767),.UNSPECIFIED.,.F.,.F.)
B_SPLINE_CURVE_WITH_KNOTS((3,3),(3.79303994872322,5.27057234608318),
 .UNSPECIFIED.)
CURVE()
GEOMETRIC_REPRESENTATION_ITEM()
RATIONAL_B_SPLINE_CURVE((1.89810041873941,1.89810041873941,1.76182294006033))
REPRESENTATION_ITEM('')
);
#568=(
BOUNDED_CURVE()
B_SPLINE_CURVE(2,(#32771,#32772,#32773),.UNSPECIFIED.,.F.,.F.)
B_SPLINE_CURVE_WITH_KNOTS((3,3),(-3.79303994872322,-2.31550755136326),
 .UNSPECIFIED.)
CURVE()
GEOMETRIC_REPRESENTATION_ITEM()
RATIONAL_B_SPLINE_CURVE((1.89810041873941,1.89810041873941,1.76182294006033))
REPRESENTATION_ITEM('')
);
#569=(
BOUNDED_CURVE()
B_SPLINE_CURVE(2,(#32774,#32775,#32776),.UNSPECIFIED.,.F.,.F.)
B_SPLINE_CURVE_WITH_KNOTS((3,3),(-5.27057234608318,-3.79303994872322),
 .UNSPECIFIED.)
CURVE()
GEOMETRIC_REPRESENTATION_ITEM()
RATIONAL_B_SPLINE_CURVE((1.76182294006033,1.89810041873941,1.89810041873941))
REPRESENTATION_ITEM('')
);
#570=(
BOUNDED_CURVE()
B_SPLINE_CURVE(2,(#32779,#32780,#32781),.UNSPECIFIED.,.F.,.F.)
B_SPLINE_CURVE_WITH_KNOTS((3,3),(2.31550755136325,3.79303994872323),
 .UNSPECIFIED.)
CURVE()
GEOMETRIC_REPRESENTATION_ITEM()
RATIONAL_B_SPLINE_CURVE((1.76182294006033,1.89810041873942,1.89810041873942))
REPRESENTATION_ITEM('')
);
#571=(
BOUNDED_CURVE()
B_SPLINE_CURVE(2,(#32782,#32783,#32784),.UNSPECIFIED.,.F.,.F.)
B_SPLINE_CURVE_WITH_KNOTS((3,3),(3.79303994872323,5.27057234608319),
 .UNSPECIFIED.)
CURVE()
GEOMETRIC_REPRESENTATION_ITEM()
RATIONAL_B_SPLINE_CURVE((1.89810041873942,1.89810041873942,1.76182294006033))
REPRESENTATION_ITEM('')
);
#572=(
BOUNDED_CURVE()
B_SPLINE_CURVE(2,(#32786,#32787,#32788),.UNSPECIFIED.,.F.,.F.)
B_SPLINE_CURVE_WITH_KNOTS((3,3),(-3.79303994872322,-2.31550755136325),
 .UNSPECIFIED.)
CURVE()
GEOMETRIC_REPRESENTATION_ITEM()
RATIONAL_B_SPLINE_CURVE((1.89810041873942,1.89810041873942,1.76182294006033))
REPRESENTATION_ITEM('')
);
#573=(
BOUNDED_CURVE()
B_SPLINE_CURVE(2,(#32789,#32790,#32791),.UNSPECIFIED.,.F.,.F.)
B_SPLINE_CURVE_WITH_KNOTS((3,3),(-5.2705723460832,-3.79303994872322),
 .UNSPECIFIED.)
CURVE()
GEOMETRIC_REPRESENTATION_ITEM()
RATIONAL_B_SPLINE_CURVE((1.76182294006033,1.89810041873942,1.89810041873942))
REPRESENTATION_ITEM('')
);
#625=CONICAL_SURFACE('',#17066,8.,0.95993108859688);
#626=CONICAL_SURFACE('',#17069,6.9,0.95993108859688);
#627=CONICAL_SURFACE('',#17093,13.5,1.0471975511966);
#628=CONICAL_SURFACE('',#17094,13.5,1.0471975511966);
#629=CONICAL_SURFACE('',#17095,13.5,1.0471975511966);
#630=CONICAL_SURFACE('',#17096,13.5,1.0471975511966);
#631=CONICAL_SURFACE('',#17097,13.5,1.0471975511966);
#632=CONICAL_SURFACE('',#17098,13.5,1.0471975511966);
#633=CONICAL_SURFACE('',#17099,13.5,1.0471975511966);
#634=CONICAL_SURFACE('',#17100,13.5,1.0471975511966);
#635=CONICAL_SURFACE('',#17101,13.5,1.0471975511966);
#636=CONICAL_SURFACE('',#17102,13.5,1.0471975511966);
#637=CONICAL_SURFACE('',#17103,13.5,1.0471975511966);
#638=CONICAL_SURFACE('',#17104,13.5,1.0471975511966);
#685=SHAPE_REPRESENTATION_RELATIONSHIP('SRR','None',#33027,#699);
#699=ADVANCED_BREP_SHAPE_REPRESENTATION('',(#1468),#32902);
#1062=CIRCLE('',#17063,8.);
#1063=CIRCLE('',#17064,8.);
#1064=CIRCLE('',#17065,8.);
#1065=CIRCLE('',#17067,7.);
#1066=CIRCLE('',#17068,7.);
#1067=CIRCLE('',#17070,7.);
#1068=CIRCLE('',#17071,8.);
#1069=CIRCLE('',#17080,13.5);
#1070=CIRCLE('',#17081,13.5);
#1071=CIRCLE('',#17082,13.5);
#1072=CIRCLE('',#17083,13.5);
#1073=CIRCLE('',#17084,13.5);
#1074=CIRCLE('',#17085,13.5);
#1075=CIRCLE('',#17087,13.5);
#1076=CIRCLE('',#17088,13.5);
#1077=CIRCLE('',#17089,13.5);
#1078=CIRCLE('',#17090,13.5);
#1079=CIRCLE('',#17091,13.5);
#1080=CIRCLE('',#17092,13.5);
#1289=CYLINDRICAL_SURFACE('',#17062,8.);
#1290=CYLINDRICAL_SURFACE('',#17072,7.);
#1379=STYLED_ITEM('',(#33099),#1468);
#1468=MANIFOLD_SOLID_BREP('Body1',#15627);
#1674=FACE_BOUND('',#3658,.T.);
#1675=FACE_BOUND('',#3660,.T.);
#2547=FACE_OUTER_BOUND('',#3647,.T.);
#2548=FACE_OUTER_BOUND('',#3648,.T.);
#2549=FACE_OUTER_BOUND('',#3649,.T.);
#2550=FACE_OUTER_BOUND('',#3650,.T.);
#2551=FACE_OUTER_BOUND('',#3651,.T.);
#2552=FACE_OUTER_BOUND('',#3652,.T.);
#2553=FACE_OUTER_BOUND('',#3653,.T.);
#2554=FACE_OUTER_BOUND('',#3654,.T.);
#2555=FACE_OUTER_BOUND('',#3655,.T.);
#2556=FACE_OUTER_BOUND('',#3656,.T.);
#2557=FACE_OUTER_BOUND('',#3657,.T.);
#2558=FACE_OUTER_BOUND('',#3659,.T.);
#2559=FACE_OUTER_BOUND('',#3661,.T.);
#2560=FACE_OUTER_BOUND('',#3662,.T.);
#2561=FACE_OUTER_BOUND('',#3663,.T.);
#2562=FACE_OUTER_BOUND('',#3664,.T.);
#2563=FACE_OUTER_BOUND('',#3665,.T.);
#2564=FACE_OUTER_BOUND('',#3666,.T.);
#2565=FACE_OUTER_BOUND('',#3667,.T.);
#2566=FACE_OUTER_BOUND('',#3668,.T.);
#2567=FACE_OUTER_BOUND('',#3669,.T.);
#2568=FACE_OUTER_BOUND('',#3670,.T.);
#2569=FACE_OUTER_BOUND('',#3671,.T.);
#2570=FACE_OUTER_BOUND('',#3672,.T.);
#3647=EDGE_LOOP('',(#13941,#13942,#13943,#13944,#13945));
#3648=EDGE_LOOP('',(#13946,#13947,#13948,#13949,#13950,#13951));
#3649=EDGE_LOOP('',(#13952,#13953,#13954,#13955));
#3650=EDGE_LOOP('',(#13956,#13957,#13958,#13959,#13960));
#3651=EDGE_LOOP('',(#13961,#13962,#13963,#13964,#13965,#13966));
#3652=EDGE_LOOP('',(#13967,#13968,#13969,#13970,#13971,#13972));
#3653=EDGE_LOOP('',(#13973,#13974,#13975,#13976,#13977,#13978));
#3654=EDGE_LOOP('',(#13979,#13980,#13981,#13982,#13983,#13984));
#3655=EDGE_LOOP('',(#13985,#13986,#13987,#13988,#13989,#13990));
#3656=EDGE_LOOP('',(#13991,#13992,#13993,#13994,#13995,#13996));
#3657=EDGE_LOOP('',(#13997,#13998,#13999,#14000,#14001,#14002));
#3658=EDGE_LOOP('',(#14003));
#3659=EDGE_LOOP('',(#14004,#14005,#14006,#14007,#14008,#14009));
#3660=EDGE_LOOP('',(#14010));
#3661=EDGE_LOOP('',(#14011,#14012,#14013));
#3662=EDGE_LOOP('',(#14014,#14015,#14016));
#3663=EDGE_LOOP('',(#14017,#14018,#14019));
#3664=EDGE_LOOP('',(#14020,#14021,#14022));
#3665=EDGE_LOOP('',(#14023,#14024,#14025));
#3666=EDGE_LOOP('',(#14026,#14027,#14028));
#3667=EDGE_LOOP('',(#14029,#14030,#14031));
#3668=EDGE_LOOP('',(#14032,#14033,#14034));
#3669=EDGE_LOOP('',(#14035,#14036,#14037));
#3670=EDGE_LOOP('',(#14038,#14039,#14040));
#3671=EDGE_LOOP('',(#14041,#14042,#14043));
#3672=EDGE_LOOP('',(#14044,#14045,#14046));
#5067=LINE('',#32666,#6471);
#5068=LINE('',#32674,#6472);
#5069=LINE('',#32680,#6473);
#5070=LINE('',#32683,#6474);
#5071=LINE('',#32687,#6475);
#5072=LINE('',#32697,#6476);
#5073=LINE('',#32715,#6477);
#5074=LINE('',#32730,#6478);
#5075=LINE('',#32751,#6479);
#5076=LINE('',#32769,#6480);
#6471=VECTOR('',#21113,8.);
#6472=VECTOR('',#21122,8.);
#6473=VECTOR('',#21129,6.9);
#6474=VECTOR('',#21134,7.);
#6475=VECTOR('',#21137,1000.);
#6476=VECTOR('',#21138,1000.);
#6477=VECTOR('',#21141,1000.);
#6478=VECTOR('',#21144,1000.);
#6479=VECTOR('',#21147,1000.);
#6480=VECTOR('',#21150,1000.);
#7806=VERTEX_POINT('',#32663);
#7807=VERTEX_POINT('',#32665);
#7808=VERTEX_POINT('',#32667);
#7809=VERTEX_POINT('',#32671);
#7810=VERTEX_POINT('',#32672);
#7811=VERTEX_POINT('',#32677);
#7812=VERTEX_POINT('',#32679);
#7813=VERTEX_POINT('',#32685);
#7814=VERTEX_POINT('',#32686);
#7815=VERTEX_POINT('',#32688);
#7816=VERTEX_POINT('',#32692);
#7817=VERTEX_POINT('',#32696);
#7818=VERTEX_POINT('',#32698);
#7819=VERTEX_POINT('',#32706);
#7820=VERTEX_POINT('',#32710);
#7821=VERTEX_POINT('',#32714);
#7822=VERTEX_POINT('',#32716);
#7823=VERTEX_POINT('',#32724);
#7824=VERTEX_POINT('',#32725);
#7825=VERTEX_POINT('',#32729);
#7826=VERTEX_POINT('',#32731);
#7827=VERTEX_POINT('',#32742);
#7828=VERTEX_POINT('',#32746);
#7829=VERTEX_POINT('',#32750);
#7830=VERTEX_POINT('',#32752);
#7831=VERTEX_POINT('',#32760);
#7832=VERTEX_POINT('',#32764);
#7833=VERTEX_POINT('',#32768);
#7834=VERTEX_POINT('',#32770);
#7835=VERTEX_POINT('',#32778);
#7836=VERTEX_POINT('',#32785);
#9854=EDGE_CURVE('',#7806,#7806,#1062,.T.);
#9855=EDGE_CURVE('',#7806,#7807,#5067,.T.);
#9856=EDGE_CURVE('',#7807,#7808,#1063,.T.);
#9857=EDGE_CURVE('',#7808,#7807,#1064,.T.);
#9858=EDGE_CURVE('',#7809,#7810,#1065,.T.);
#9859=EDGE_CURVE('',#7810,#7808,#5068,.T.);
#9860=EDGE_CURVE('',#7810,#7809,#1066,.T.);
#9861=EDGE_CURVE('',#7811,#7811,#1067,.T.);
#9862=EDGE_CURVE('',#7811,#7812,#5069,.T.);
#9863=EDGE_CURVE('',#7812,#7812,#1068,.T.);
#9864=EDGE_CURVE('',#7809,#7811,#5070,.T.);
#9865=EDGE_CURVE('',#7813,#7814,#5071,.T.);
#9866=EDGE_CURVE('',#7814,#7815,#550,.T.);
#9867=EDGE_CURVE('',#7815,#7816,#551,.T.);
#9868=EDGE_CURVE('',#7817,#7816,#5072,.T.);
#9869=EDGE_CURVE('',#7818,#7817,#552,.T.);
#9870=EDGE_CURVE('',#7813,#7818,#553,.T.);
#9871=EDGE_CURVE('',#7816,#7819,#554,.T.);
#9872=EDGE_CURVE('',#7819,#7820,#555,.T.);
#9873=EDGE_CURVE('',#7821,#7820,#5073,.T.);
#9874=EDGE_CURVE('',#7822,#7821,#556,.T.);
#9875=EDGE_CURVE('',#7817,#7822,#557,.T.);
#9876=EDGE_CURVE('',#7823,#7824,#558,.T.);
#9877=EDGE_CURVE('',#7825,#7823,#5074,.T.);
#9878=EDGE_CURVE('',#7825,#7826,#559,.T.);
#9879=EDGE_CURVE('',#7826,#7821,#560,.T.);
#9880=EDGE_CURVE('',#7824,#7820,#561,.T.);
#9881=EDGE_CURVE('',#7823,#7827,#562,.T.);
#9882=EDGE_CURVE('',#7827,#7828,#563,.T.);
#9883=EDGE_CURVE('',#7829,#7828,#5075,.T.);
#9884=EDGE_CURVE('',#7830,#7829,#564,.T.);
#9885=EDGE_CURVE('',#7825,#7830,#565,.T.);
#9886=EDGE_CURVE('',#7828,#7831,#566,.T.);
#9887=EDGE_CURVE('',#7831,#7832,#567,.T.);
#9888=EDGE_CURVE('',#7833,#7832,#5076,.T.);
#9889=EDGE_CURVE('',#7834,#7833,#568,.T.);
#9890=EDGE_CURVE('',#7829,#7834,#569,.T.);
#9891=EDGE_CURVE('',#7832,#7835,#570,.T.);
#9892=EDGE_CURVE('',#7835,#7814,#571,.T.);
#9893=EDGE_CURVE('',#7836,#7813,#572,.T.);
#9894=EDGE_CURVE('',#7833,#7836,#573,.T.);
#9895=EDGE_CURVE('',#7835,#7815,#1069,.T.);
#9896=EDGE_CURVE('',#7831,#7835,#1070,.T.);
#9897=EDGE_CURVE('',#7827,#7831,#1071,.T.);
#9898=EDGE_CURVE('',#7824,#7827,#1072,.T.);
#9899=EDGE_CURVE('',#7824,#7819,#1073,.T.);
#9900=EDGE_CURVE('',#7815,#7819,#1074,.T.);
#9901=EDGE_CURVE('',#7836,#7834,#1075,.T.);
#9902=EDGE_CURVE('',#7818,#7836,#1076,.T.);
#9903=EDGE_CURVE('',#7822,#7818,#1077,.T.);
#9904=EDGE_CURVE('',#7826,#7822,#1078,.T.);
#9905=EDGE_CURVE('',#7830,#7826,#1079,.T.);
#9906=EDGE_CURVE('',#7834,#7830,#1080,.T.);
#13941=ORIENTED_EDGE('',*,*,#9854,.F.);
#13942=ORIENTED_EDGE('',*,*,#9855,.T.);
#13943=ORIENTED_EDGE('',*,*,#9856,.T.);
#13944=ORIENTED_EDGE('',*,*,#9857,.T.);
#13945=ORIENTED_EDGE('',*,*,#9855,.F.);
#13946=ORIENTED_EDGE('',*,*,#9858,.T.);
#13947=ORIENTED_EDGE('',*,*,#9859,.T.);
#13948=ORIENTED_EDGE('',*,*,#9856,.F.);
#13949=ORIENTED_EDGE('',*,*,#9857,.F.);
#13950=ORIENTED_EDGE('',*,*,#9859,.F.);
#13951=ORIENTED_EDGE('',*,*,#9860,.T.);
#13952=ORIENTED_EDGE('',*,*,#9861,.T.);
#13953=ORIENTED_EDGE('',*,*,#9862,.T.);
#13954=ORIENTED_EDGE('',*,*,#9863,.T.);
#13955=ORIENTED_EDGE('',*,*,#9862,.F.);
#13956=ORIENTED_EDGE('',*,*,#9858,.F.);
#13957=ORIENTED_EDGE('',*,*,#9864,.T.);
#13958=ORIENTED_EDGE('',*,*,#9861,.F.);
#13959=ORIENTED_EDGE('',*,*,#9864,.F.);
#13960=ORIENTED_EDGE('',*,*,#9860,.F.);
#13961=ORIENTED_EDGE('',*,*,#9865,.T.);
#13962=ORIENTED_EDGE('',*,*,#9866,.T.);
#13963=ORIENTED_EDGE('',*,*,#9867,.T.);
#13964=ORIENTED_EDGE('',*,*,#9868,.F.);
#13965=ORIENTED_EDGE('',*,*,#9869,.F.);
#13966=ORIENTED_EDGE('',*,*,#9870,.F.);
#13967=ORIENTED_EDGE('',*,*,#9868,.T.);
#13968=ORIENTED_EDGE('',*,*,#9871,.T.);
#13969=ORIENTED_EDGE('',*,*,#9872,.T.);
#13970=ORIENTED_EDGE('',*,*,#9873,.F.);
#13971=ORIENTED_EDGE('',*,*,#9874,.F.);
#13972=ORIENTED_EDGE('',*,*,#9875,.F.);
#13973=ORIENTED_EDGE('',*,*,#9876,.F.);
#13974=ORIENTED_EDGE('',*,*,#9877,.F.);
#13975=ORIENTED_EDGE('',*,*,#9878,.T.);
#13976=ORIENTED_EDGE('',*,*,#9879,.T.);
#13977=ORIENTED_EDGE('',*,*,#9873,.T.);
#13978=ORIENTED_EDGE('',*,*,#9880,.F.);
#13979=ORIENTED_EDGE('',*,*,#9877,.T.);
#13980=ORIENTED_EDGE('',*,*,#9881,.T.);
#13981=ORIENTED_EDGE('',*,*,#9882,.T.);
#13982=ORIENTED_EDGE('',*,*,#9883,.F.);
#13983=ORIENTED_EDGE('',*,*,#9884,.F.);
#13984=ORIENTED_EDGE('',*,*,#9885,.F.);
#13985=ORIENTED_EDGE('',*,*,#9883,.T.);
#13986=ORIENTED_EDGE('',*,*,#9886,.T.);
#13987=ORIENTED_EDGE('',*,*,#9887,.T.);
#13988=ORIENTED_EDGE('',*,*,#9888,.F.);
#13989=ORIENTED_EDGE('',*,*,#9889,.F.);
#13990=ORIENTED_EDGE('',*,*,#9890,.F.);
#13991=ORIENTED_EDGE('',*,*,#9888,.T.);
#13992=ORIENTED_EDGE('',*,*,#9891,.T.);
#13993=ORIENTED_EDGE('',*,*,#9892,.T.);
#13994=ORIENTED_EDGE('',*,*,#9865,.F.);
#13995=ORIENTED_EDGE('',*,*,#9893,.F.);
#13996=ORIENTED_EDGE('',*,*,#9894,.F.);
#13997=ORIENTED_EDGE('',*,*,#9895,.F.);
#13998=ORIENTED_EDGE('',*,*,#9896,.F.);
#13999=ORIENTED_EDGE('',*,*,#9897,.F.);
#14000=ORIENTED_EDGE('',*,*,#9898,.F.);
#14001=ORIENTED_EDGE('',*,*,#9899,.T.);
#14002=ORIENTED_EDGE('',*,*,#9900,.F.);
#14003=ORIENTED_EDGE('',*,*,#9863,.F.);
#14004=ORIENTED_EDGE('',*,*,#9901,.F.);
#14005=ORIENTED_EDGE('',*,*,#9902,.F.);
#14006=ORIENTED_EDGE('',*,*,#9903,.F.);
#14007=ORIENTED_EDGE('',*,*,#9904,.F.);
#14008=ORIENTED_EDGE('',*,*,#9905,.F.);
#14009=ORIENTED_EDGE('',*,*,#9906,.F.);
#14010=ORIENTED_EDGE('',*,*,#9854,.T.);
#14011=ORIENTED_EDGE('',*,*,#9870,.T.);
#14012=ORIENTED_EDGE('',*,*,#9902,.T.);
#14013=ORIENTED_EDGE('',*,*,#9893,.T.);
#14014=ORIENTED_EDGE('',*,*,#9869,.T.);
#14015=ORIENTED_EDGE('',*,*,#9875,.T.);
#14016=ORIENTED_EDGE('',*,*,#9903,.T.);
#14017=ORIENTED_EDGE('',*,*,#9874,.T.);
#14018=ORIENTED_EDGE('',*,*,#9879,.F.);
#14019=ORIENTED_EDGE('',*,*,#9904,.T.);
#14020=ORIENTED_EDGE('',*,*,#9885,.T.);
#14021=ORIENTED_EDGE('',*,*,#9905,.T.);
#14022=ORIENTED_EDGE('',*,*,#9878,.F.);
#14023=ORIENTED_EDGE('',*,*,#9884,.T.);
#14024=ORIENTED_EDGE('',*,*,#9890,.T.);
#14025=ORIENTED_EDGE('',*,*,#9906,.T.);
#14026=ORIENTED_EDGE('',*,*,#9889,.T.);
#14027=ORIENTED_EDGE('',*,*,#9894,.T.);
#14028=ORIENTED_EDGE('',*,*,#9901,.T.);
#14029=ORIENTED_EDGE('',*,*,#9896,.T.);
#14030=ORIENTED_EDGE('',*,*,#9891,.F.);
#14031=ORIENTED_EDGE('',*,*,#9887,.F.);
#14032=ORIENTED_EDGE('',*,*,#9897,.T.);
#14033=ORIENTED_EDGE('',*,*,#9886,.F.);
#14034=ORIENTED_EDGE('',*,*,#9882,.F.);
#14035=ORIENTED_EDGE('',*,*,#9876,.T.);
#14036=ORIENTED_EDGE('',*,*,#9898,.T.);
#14037=ORIENTED_EDGE('',*,*,#9881,.F.);
#14038=ORIENTED_EDGE('',*,*,#9899,.F.);
#14039=ORIENTED_EDGE('',*,*,#9880,.T.);
#14040=ORIENTED_EDGE('',*,*,#9872,.F.);
#14041=ORIENTED_EDGE('',*,*,#9900,.T.);
#14042=ORIENTED_EDGE('',*,*,#9871,.F.);
#14043=ORIENTED_EDGE('',*,*,#9867,.F.);
#14044=ORIENTED_EDGE('',*,*,#9892,.F.);
#14045=ORIENTED_EDGE('',*,*,#9895,.T.);
#14046=ORIENTED_EDGE('',*,*,#9866,.F.);
#14636=PLANE('',#17073);
#14637=PLANE('',#17074);
#14638=PLANE('',#17075);
#14639=PLANE('',#17076);
#14640=PLANE('',#17077);
#14641=PLANE('',#17078);
#14642=PLANE('',#17079);
#14643=PLANE('',#17086);
#15515=ADVANCED_FACE('',(#2547),#1289,.F.);
#15516=ADVANCED_FACE('',(#2548),#625,.F.);
#15517=ADVANCED_FACE('',(#2549),#626,.F.);
#15518=ADVANCED_FACE('',(#2550),#1290,.F.);
#15519=ADVANCED_FACE('',(#2551),#14636,.T.);
#15520=ADVANCED_FACE('',(#2552),#14637,.T.);
#15521=ADVANCED_FACE('',(#2553),#14638,.F.);
#15522=ADVANCED_FACE('',(#2554),#14639,.T.);
#15523=ADVANCED_FACE('',(#2555),#14640,.T.);
#15524=ADVANCED_FACE('',(#2556),#14641,.T.);
#15525=ADVANCED_FACE('',(#2557,#1674),#14642,.F.);
#15526=ADVANCED_FACE('',(#2558,#1675),#14643,.T.);
#15527=ADVANCED_FACE('',(#2559),#627,.T.);
#15528=ADVANCED_FACE('',(#2560),#628,.T.);
#15529=ADVANCED_FACE('',(#2561),#629,.T.);
#15530=ADVANCED_FACE('',(#2562),#630,.T.);
#15531=ADVANCED_FACE('',(#2563),#631,.T.);
#15532=ADVANCED_FACE('',(#2564),#632,.T.);
#15533=ADVANCED_FACE('',(#2565),#633,.T.);
#15534=ADVANCED_FACE('',(#2566),#634,.T.);
#15535=ADVANCED_FACE('',(#2567),#635,.T.);
#15536=ADVANCED_FACE('',(#2568),#636,.T.);
#15537=ADVANCED_FACE('',(#2569),#637,.T.);
#15538=ADVANCED_FACE('',(#2570),#638,.T.);
#15627=CLOSED_SHELL('',(#15515,#15516,#15517,#15518,#15519,#15520,#15521,
#15522,#15523,#15524,#15525,#15526,#15527,#15528,#15529,#15530,#15531,#15532,
#15533,#15534,#15535,#15536,#15537,#15538));
#17061=AXIS2_PLACEMENT_3D('',#32661,#21107,#21108);
#17062=AXIS2_PLACEMENT_3D('',#32662,#21109,#21110);
#17063=AXIS2_PLACEMENT_3D('',#32664,#21111,#21112);
#17064=AXIS2_PLACEMENT_3D('',#32668,#21114,#21115);
#17065=AXIS2_PLACEMENT_3D('',#32669,#21116,#21117);
#17066=AXIS2_PLACEMENT_3D('',#32670,#21118,#21119);
#17067=AXIS2_PLACEMENT_3D('',#32673,#21120,#21121);
#17068=AXIS2_PLACEMENT_3D('',#32675,#21123,#21124);
#17069=AXIS2_PLACEMENT_3D('',#32676,#21125,#21126);
#17070=AXIS2_PLACEMENT_3D('',#32678,#21127,#21128);
#17071=AXIS2_PLACEMENT_3D('',#32681,#21130,#21131);
#17072=AXIS2_PLACEMENT_3D('',#32682,#21132,#21133);
#17073=AXIS2_PLACEMENT_3D('',#32684,#21135,#21136);
#17074=AXIS2_PLACEMENT_3D('',#32705,#21139,#21140);
#17075=AXIS2_PLACEMENT_3D('',#32723,#21142,#21143);
#17076=AXIS2_PLACEMENT_3D('',#32741,#21145,#21146);
#17077=AXIS2_PLACEMENT_3D('',#32759,#21148,#21149);
#17078=AXIS2_PLACEMENT_3D('',#32777,#21151,#21152);
#17079=AXIS2_PLACEMENT_3D('',#32792,#21153,#21154);
#17080=AXIS2_PLACEMENT_3D('',#32793,#21155,#21156);
#17081=AXIS2_PLACEMENT_3D('',#32794,#21157,#21158);
#17082=AXIS2_PLACEMENT_3D('',#32795,#21159,#21160);
#17083=AXIS2_PLACEMENT_3D('',#32796,#21161,#21162);
#17084=AXIS2_PLACEMENT_3D('',#32797,#21163,#21164);
#17085=AXIS2_PLACEMENT_3D('',#32798,#21165,#21166);
#17086=AXIS2_PLACEMENT_3D('',#32799,#21167,#21168);
#17087=AXIS2_PLACEMENT_3D('',#32800,#21169,#21170);
#17088=AXIS2_PLACEMENT_3D('',#32801,#21171,#21172);
#17089=AXIS2_PLACEMENT_3D('',#32802,#21173,#21174);
#17090=AXIS2_PLACEMENT_3D('',#32803,#21175,#21176);
#17091=AXIS2_PLACEMENT_3D('',#32804,#21177,#21178);
#17092=AXIS2_PLACEMENT_3D('',#32805,#21179,#21180);
#17093=AXIS2_PLACEMENT_3D('',#32806,#21181,#21182);
#17094=AXIS2_PLACEMENT_3D('',#32807,#21183,#21184);
#17095=AXIS2_PLACEMENT_3D('',#32808,#21185,#21186);
#17096=AXIS2_PLACEMENT_3D('',#32809,#21187,#21188);
#17097=AXIS2_PLACEMENT_3D('',#32810,#21189,#21190);
#17098=AXIS2_PLACEMENT_3D('',#32811,#21191,#21192);
#17099=AXIS2_PLACEMENT_3D('',#32812,#21193,#21194);
#17100=AXIS2_PLACEMENT_3D('',#32813,#21195,#21196);
#17101=AXIS2_PLACEMENT_3D('',#32814,#21197,#21198);
#17102=AXIS2_PLACEMENT_3D('',#32815,#21199,#21200);
#17103=AXIS2_PLACEMENT_3D('',#32816,#21201,#21202);
#17104=AXIS2_PLACEMENT_3D('',#32817,#21203,#21204);
#21107=DIRECTION('axis',(0.,0.,1.));
#21108=DIRECTION('refdir',(1.,0.,0.));
#21109=DIRECTION('center_axis',(0.,0.,1.));
#21110=DIRECTION('ref_axis',(1.,0.,0.));
#21111=DIRECTION('center_axis',(0.,0.,1.));
#21112=DIRECTION('ref_axis',(-1.,0.,0.));
#21113=DIRECTION('',(0.,0.,1.));
#21114=DIRECTION('center_axis',(0.,0.,1.));
#21115=DIRECTION('ref_axis',(1.,0.,0.));
#21116=DIRECTION('center_axis',(0.,0.,1.));
#21117=DIRECTION('ref_axis',(1.,0.,0.));
#21118=DIRECTION('center_axis',(0.,0.,-1.));
#21119=DIRECTION('ref_axis',(-1.,0.,0.));
#21120=DIRECTION('center_axis',(0.,0.,1.));
#21121=DIRECTION('ref_axis',(-1.,0.,0.));
#21122=DIRECTION('',(0.819152044288991,-1.00317192905352E-16,-0.573576436351047));
#21123=DIRECTION('center_axis',(0.,0.,1.));
#21124=DIRECTION('ref_axis',(-1.,0.,0.));
#21125=DIRECTION('center_axis',(0.,0.,1.));
#21126=DIRECTION('ref_axis',(1.,0.,0.));
#21127=DIRECTION('center_axis',(0.,0.,-1.));
#21128=DIRECTION('ref_axis',(1.,0.,0.));
#21129=DIRECTION('',(-0.819152044288991,-1.00317192905352E-16,0.573576436351047));
#21130=DIRECTION('center_axis',(0.,0.,1.));
#21131=DIRECTION('ref_axis',(1.,0.,0.));
#21132=DIRECTION('center_axis',(0.,0.,1.));
#21133=DIRECTION('ref_axis',(1.,0.,0.));
#21134=DIRECTION('',(0.,0.,1.));
#21135=DIRECTION('center_axis',(-0.500000000000001,0.866025403784438,0.));
#21136=DIRECTION('ref_axis',(-0.866025403784438,-0.500000000000001,0.));
#21137=DIRECTION('',(0.,0.,1.));
#21138=DIRECTION('',(0.,0.,1.));
#21139=DIRECTION('center_axis',(0.500000000000001,0.866025403784438,0.));
#21140=DIRECTION('ref_axis',(-0.866025403784438,0.500000000000001,0.));
#21141=DIRECTION('',(0.,0.,1.));
#21142=DIRECTION('center_axis',(-1.,0.,0.));
#21143=DIRECTION('ref_axis',(0.,0.,1.));
#21144=DIRECTION('',(0.,0.,1.));
#21145=DIRECTION('center_axis',(0.500000000000001,-0.866025403784438,0.));
#21146=DIRECTION('ref_axis',(0.866025403784438,0.500000000000001,0.));
#21147=DIRECTION('',(0.,0.,1.));
#21148=DIRECTION('center_axis',(-0.500000000000001,-0.866025403784438,0.));
#21149=DIRECTION('ref_axis',(0.866025403784438,-0.500000000000001,0.));
#21150=DIRECTION('',(0.,0.,1.));
#21151=DIRECTION('center_axis',(-1.,0.,0.));
#21152=DIRECTION('ref_axis',(0.,0.,1.));
#21153=DIRECTION('center_axis',(0.,0.,-1.));
#21154=DIRECTION('ref_axis',(-1.,0.,0.));
#21155=DIRECTION('center_axis',(0.,0.,-1.));
#21156=DIRECTION('ref_axis',(-1.,0.,0.));
#21157=DIRECTION('center_axis',(0.,0.,-1.));
#21158=DIRECTION('ref_axis',(-1.,0.,0.));
#21159=DIRECTION('center_axis',(0.,0.,-1.));
#21160=DIRECTION('ref_axis',(-1.,0.,0.));
#21161=DIRECTION('center_axis',(0.,0.,-1.));
#21162=DIRECTION('ref_axis',(-1.,0.,0.));
#21163=DIRECTION('center_axis',(0.,0.,1.));
#21164=DIRECTION('ref_axis',(1.,0.,0.));
#21165=DIRECTION('center_axis',(0.,0.,-1.));
#21166=DIRECTION('ref_axis',(-1.,0.,0.));
#21167=DIRECTION('center_axis',(0.,0.,-1.));
#21168=DIRECTION('ref_axis',(-1.,0.,0.));
#21169=DIRECTION('center_axis',(0.,0.,1.));
#21170=DIRECTION('ref_axis',(-1.,0.,0.));
#21171=DIRECTION('center_axis',(0.,0.,1.));
#21172=DIRECTION('ref_axis',(-1.,-8.88178419700125E-16,0.));
#21173=DIRECTION('center_axis',(0.,0.,1.));
#21174=DIRECTION('ref_axis',(-1.,3.5527136788005E-15,0.));
#21175=DIRECTION('center_axis',(0.,0.,1.));
#21176=DIRECTION('ref_axis',(1.,0.,0.));
#21177=DIRECTION('center_axis',(0.,0.,1.));
#21178=DIRECTION('ref_axis',(-1.,1.77635683940025E-15,0.));
#21179=DIRECTION('center_axis',(0.,0.,1.));
#21180=DIRECTION('ref_axis',(-1.,0.,0.));
#21181=DIRECTION('center_axis',(0.,0.,1.));
#21182=DIRECTION('ref_axis',(1.,0.,0.));
#21183=DIRECTION('center_axis',(0.,0.,1.));
#21184=DIRECTION('ref_axis',(1.,0.,0.));
#21185=DIRECTION('center_axis',(0.,0.,1.));
#21186=DIRECTION('ref_axis',(1.,0.,0.));
#21187=DIRECTION('center_axis',(0.,0.,1.));
#21188=DIRECTION('ref_axis',(1.,0.,0.));
#21189=DIRECTION('center_axis',(0.,0.,1.));
#21190=DIRECTION('ref_axis',(1.,0.,0.));
#21191=DIRECTION('center_axis',(0.,0.,1.));
#21192=DIRECTION('ref_axis',(1.,0.,0.));
#21193=DIRECTION('center_axis',(0.,0.,-1.));
#21194=DIRECTION('ref_axis',(-1.,0.,0.));
#21195=DIRECTION('center_axis',(0.,0.,-1.));
#21196=DIRECTION('ref_axis',(-1.,0.,0.));
#21197=DIRECTION('center_axis',(0.,0.,-1.));
#21198=DIRECTION('ref_axis',(-1.,0.,0.));
#21199=DIRECTION('center_axis',(0.,0.,-1.));
#21200=DIRECTION('ref_axis',(-1.,0.,0.));
#21201=DIRECTION('center_axis',(0.,0.,-1.));
#21202=DIRECTION('ref_axis',(-1.,0.,0.));
#21203=DIRECTION('center_axis',(0.,0.,-1.));
#21204=DIRECTION('ref_axis',(-1.,0.,0.));
#32661=CARTESIAN_POINT('',(0.,0.,0.));
#32662=CARTESIAN_POINT('Origin',(0.,0.,-25.0375057290932));
#32663=CARTESIAN_POINT('',(-8.,-9.79717439317883E-16,-13.));
#32664=CARTESIAN_POINT('Origin',(0.,0.,-13.));
#32665=CARTESIAN_POINT('',(-8.,-9.79717439317883E-16,-12.9746));
#32666=CARTESIAN_POINT('',(-8.,-9.79717439317883E-16,-25.0375057290932));
#32667=CARTESIAN_POINT('',(8.,9.79717439317883E-16,-12.9746));
#32668=CARTESIAN_POINT('Origin',(0.,0.,-12.9746));
#32669=CARTESIAN_POINT('Origin',(0.,0.,-12.9746));
#32670=CARTESIAN_POINT('Origin',(0.,0.,-12.9746));
#32671=CARTESIAN_POINT('',(-7.,8.57252759403147E-16,-12.2743924617903));
#32672=CARTESIAN_POINT('',(7.,-8.57252759403147E-16,-12.2743924617903));
#32673=CARTESIAN_POINT('Origin',(0.,0.,-12.2743924617903));
#32674=CARTESIAN_POINT('',(8.,-9.79717439317883E-16,-12.9746));
#32675=CARTESIAN_POINT('Origin',(0.,0.,-12.2743924617903));
#32676=CARTESIAN_POINT('Origin',(0.,0.,-0.770228292030679));
#32677=CARTESIAN_POINT('',(-7.,-8.57252759403147E-16,-0.700207538209708));
#32678=CARTESIAN_POINT('Origin',(0.,0.,-0.700207538209708));
#32679=CARTESIAN_POINT('',(-8.,-9.79717439317883E-16,4.44089209850063E-15));
#32680=CARTESIAN_POINT('',(-6.9,-8.45006291411674E-16,-0.770228292030679));
#32681=CARTESIAN_POINT('Origin',(0.,0.,3.46944695195361E-15));
#32682=CARTESIAN_POINT('Origin',(0.,0.,-13.));
#32683=CARTESIAN_POINT('',(-7.,-8.57252759403147E-16,-13.));
#32684=CARTESIAN_POINT('Origin',(-3.60150143354614E-16,15.5884572681199,
-13.));
#32685=CARTESIAN_POINT('',(-13.5,7.79422863405999,-11.7942286340599));
#32686=CARTESIAN_POINT('',(-13.5,7.79422863405993,-1.20577136594005));
#32687=CARTESIAN_POINT('',(-13.5,7.79422863405993,-13.));
#32688=CARTESIAN_POINT('',(-6.75000000000002,11.6913429510899,0.));
#32689=CARTESIAN_POINT('Ctrl Pts',(-13.5000000000255,7.79422863404522,-1.20577136594854));
#32690=CARTESIAN_POINT('Ctrl Pts',(-9.8826859021901,9.88268590217392,3.5527136788005E-15));
#32691=CARTESIAN_POINT('Ctrl Pts',(-6.75000000000002,11.6913429510899,3.27551107229086E-15));
#32692=CARTESIAN_POINT('',(-8.67361737988404E-16,15.5884572681199,-1.20577136594007));
#32693=CARTESIAN_POINT('Ctrl Pts',(-6.75000000000002,11.6913429510899,3.27551107229086E-15));
#32694=CARTESIAN_POINT('Ctrl Pts',(-3.61731409780992,13.5000000000059,3.03751290454254E-15));
#32695=CARTESIAN_POINT('Ctrl Pts',(2.54925766410204E-11,15.5884572681346,
-1.20577136594856));
#32696=CARTESIAN_POINT('',(-8.67361737988404E-16,15.5884572681199,-11.7942286340599));
#32697=CARTESIAN_POINT('',(-3.60150143354614E-16,15.5884572681199,-13.));
#32698=CARTESIAN_POINT('',(-6.75000000000002,11.6913429510899,-13.));
#32699=CARTESIAN_POINT('Ctrl Pts',(-6.75000000000006,11.6913429510899,-13.));
#32700=CARTESIAN_POINT('Ctrl Pts',(-3.61731409780995,13.5000000000059,-13.));
#32701=CARTESIAN_POINT('Ctrl Pts',(2.54744281526666E-11,15.5884572681346,
-11.7942286340514));
#32702=CARTESIAN_POINT('Ctrl Pts',(-13.5000000000254,7.79422863404524,-11.7942286340515));
#32703=CARTESIAN_POINT('Ctrl Pts',(-9.8826859021901,9.88268590217391,-13.));
#32704=CARTESIAN_POINT('Ctrl Pts',(-6.75000000000006,11.6913429510899,-13.));
#32705=CARTESIAN_POINT('Origin',(13.5,7.79422863405994,-13.));
#32706=CARTESIAN_POINT('',(6.75000000000002,11.6913429510899,0.));
#32707=CARTESIAN_POINT('Ctrl Pts',(-2.5481990022814E-11,15.5884572681346,
-1.20577136594856));
#32708=CARTESIAN_POINT('Ctrl Pts',(3.61731409780993,13.5000000000059,1.22124532708767E-15));
#32709=CARTESIAN_POINT('Ctrl Pts',(6.75000000000003,11.6913429510899,-9.35860306368824E-16));
#32710=CARTESIAN_POINT('',(13.5,7.79422863405998,-1.20577136594007));
#32711=CARTESIAN_POINT('Ctrl Pts',(6.75000000000003,11.6913429510899,-9.35860306368824E-16));
#32712=CARTESIAN_POINT('Ctrl Pts',(9.8826859021901,9.88268590217392,-3.16615028890809E-15));
#32713=CARTESIAN_POINT('Ctrl Pts',(13.5000000000255,7.79422863404523,-1.20577136594854));
#32714=CARTESIAN_POINT('',(13.5,7.79422863405998,-11.7942286340599));
#32715=CARTESIAN_POINT('',(13.5,7.79422863405994,-13.));
#32716=CARTESIAN_POINT('',(6.75000000000002,11.6913429510899,-13.));
#32717=CARTESIAN_POINT('Ctrl Pts',(6.75000000000002,11.6913429510899,-13.));
#32718=CARTESIAN_POINT('Ctrl Pts',(9.88268590219009,9.88268590217393,-13.));
#32719=CARTESIAN_POINT('Ctrl Pts',(13.5000000000255,7.79422863404524,-11.7942286340515));
#32720=CARTESIAN_POINT('Ctrl Pts',(-2.54467012954593E-11,15.5884572681346,
-11.7942286340515));
#32721=CARTESIAN_POINT('Ctrl Pts',(3.61731409780994,13.5000000000059,-13.));
#32722=CARTESIAN_POINT('Ctrl Pts',(6.75000000000002,11.6913429510899,-13.));
#32723=CARTESIAN_POINT('Origin',(13.5,7.79422863405994,-13.));
#32724=CARTESIAN_POINT('',(13.5,-7.79422863405998,-1.20577136594007));
#32725=CARTESIAN_POINT('',(13.5,0.,0.));
#32726=CARTESIAN_POINT('Ctrl Pts',(13.5,-7.79422863408939,-1.20577136594856));
#32727=CARTESIAN_POINT('Ctrl Pts',(13.5,-3.61731409783199,-2.1094237467878E-15));
#32728=CARTESIAN_POINT('Ctrl Pts',(13.5,0.,-2.33965076592205E-15));
#32729=CARTESIAN_POINT('',(13.5,-7.79422863405998,-11.7942286340599));
#32730=CARTESIAN_POINT('',(13.5,-7.79422863405998,-13.));
#32731=CARTESIAN_POINT('',(13.5,0.,-13.));
#32732=CARTESIAN_POINT('Ctrl Pts',(13.5,-7.79422863408946,-11.7942286340514));
#32733=CARTESIAN_POINT('Ctrl Pts',(13.5,-3.61731409783202,-13.));
#32734=CARTESIAN_POINT('Ctrl Pts',(13.5,0.,-13.));
#32735=CARTESIAN_POINT('Ctrl Pts',(13.5,0.,-13.));
#32736=CARTESIAN_POINT('Ctrl Pts',(13.5,3.617314097832,-13.));
#32737=CARTESIAN_POINT('Ctrl Pts',(13.5,7.79422863408941,-11.7942286340514));
#32738=CARTESIAN_POINT('Ctrl Pts',(13.5,0.,-2.33965076592205E-15));
#32739=CARTESIAN_POINT('Ctrl Pts',(13.5,3.617314097832,-2.29321602408394E-15));
#32740=CARTESIAN_POINT('Ctrl Pts',(13.5,7.79422863408942,-1.20577136594857));
#32741=CARTESIAN_POINT('Origin',(2.2354950088892E-15,-15.5884572681199,
-13.));
#32742=CARTESIAN_POINT('',(6.75000000000002,-11.6913429510899,0.));
#32743=CARTESIAN_POINT('Ctrl Pts',(13.5000000000255,-7.79422863404527,-1.20577136594856));
#32744=CARTESIAN_POINT('Ctrl Pts',(9.88268590219011,-9.88268590217396,-2.1538326677728E-14));
#32745=CARTESIAN_POINT('Ctrl Pts',(6.75000000000003,-11.69134295109,-2.03549616635218E-14));
#32746=CARTESIAN_POINT('',(-5.72458747072346E-14,-15.5884572681199,-1.20577136594007));
#32747=CARTESIAN_POINT('Ctrl Pts',(6.75000000000003,-11.69134295109,-2.03549616635218E-14));
#32748=CARTESIAN_POINT('Ctrl Pts',(3.61731409780992,-13.500000000006,-1.8826547469893E-14));
#32749=CARTESIAN_POINT('Ctrl Pts',(-2.55036673839034E-11,-15.5884572681347,
-1.20577136594859));
#32750=CARTESIAN_POINT('',(-5.72458747072346E-14,-15.5884572681199,-11.7942286340599));
#32751=CARTESIAN_POINT('',(2.2354950088892E-15,-15.5884572681199,-13.));
#32752=CARTESIAN_POINT('',(6.75000000000002,-11.6913429510899,-13.));
#32753=CARTESIAN_POINT('Ctrl Pts',(6.75000000000008,-11.6913429510899,-13.));
#32754=CARTESIAN_POINT('Ctrl Pts',(3.61731409780995,-13.5000000000059,-13.));
#32755=CARTESIAN_POINT('Ctrl Pts',(-2.55021550098739E-11,-15.5884572681347,
-11.7942286340514));
#32756=CARTESIAN_POINT('Ctrl Pts',(13.5000000000255,-7.79422863404526,-11.7942286340514));
#32757=CARTESIAN_POINT('Ctrl Pts',(9.88268590219014,-9.88268590217394,-13.));
#32758=CARTESIAN_POINT('Ctrl Pts',(6.75000000000008,-11.6913429510899,-13.));
#32759=CARTESIAN_POINT('Origin',(-13.5,-7.79422863405998,-13.));
#32760=CARTESIAN_POINT('',(-6.75000000000002,-11.6913429510899,0.));
#32761=CARTESIAN_POINT('Ctrl Pts',(2.54255280590466E-11,-15.5884572681346,
-1.20577136594856));
#32762=CARTESIAN_POINT('Ctrl Pts',(-3.61731409780995,-13.5000000000059,
-1.96509475358653E-14));
#32763=CARTESIAN_POINT('Ctrl Pts',(-6.75000000000003,-11.6913429510899,
-1.98870315103374E-14));
#32764=CARTESIAN_POINT('',(-13.5,-7.79422863405999,-1.20577136594007));
#32765=CARTESIAN_POINT('Ctrl Pts',(-6.75000000000003,-11.6913429510899,
-1.98870315103374E-14));
#32766=CARTESIAN_POINT('Ctrl Pts',(-9.8826859021901,-9.88268590217396,-1.9578830969301E-14));
#32767=CARTESIAN_POINT('Ctrl Pts',(-13.5000000000255,-7.79422863404527,
-1.20577136594856));
#32768=CARTESIAN_POINT('',(-13.5,-7.79422863405999,-11.7942286340599));
#32769=CARTESIAN_POINT('',(-13.5,-7.79422863405998,-13.));
#32770=CARTESIAN_POINT('',(-6.75000000000002,-11.6913429510899,-13.));
#32771=CARTESIAN_POINT('Ctrl Pts',(-6.75000000000005,-11.6913429510899,
-13.));
#32772=CARTESIAN_POINT('Ctrl Pts',(-9.88268590219012,-9.88268590217395,
-13.));
#32773=CARTESIAN_POINT('Ctrl Pts',(-13.5000000000255,-7.79422863404526,
-11.7942286340514));
#32774=CARTESIAN_POINT('Ctrl Pts',(2.54068754460162E-11,-15.5884572681346,
-11.7942286340514));
#32775=CARTESIAN_POINT('Ctrl Pts',(-3.61731409780997,-13.5000000000059,
-13.));
#32776=CARTESIAN_POINT('Ctrl Pts',(-6.75000000000005,-11.6913429510899,
-13.));
#32777=CARTESIAN_POINT('Origin',(-13.5,7.79422863405993,-13.));
#32778=CARTESIAN_POINT('',(-13.5,0.,0.));
#32779=CARTESIAN_POINT('Ctrl Pts',(-13.5,-7.7942286340894,-1.20577136594856));
#32780=CARTESIAN_POINT('Ctrl Pts',(-13.5,-3.61731409783199,3.66373598126302E-15));
#32781=CARTESIAN_POINT('Ctrl Pts',(-13.5,7.48688245095054E-15,2.33965076592204E-15));
#32782=CARTESIAN_POINT('Ctrl Pts',(-13.5,7.48688245095054E-15,2.33965076592204E-15));
#32783=CARTESIAN_POINT('Ctrl Pts',(-13.5,3.61731409783197,9.09299790684234E-16));
#32784=CARTESIAN_POINT('Ctrl Pts',(-13.5,7.79422863408933,-1.20577136594854));
#32785=CARTESIAN_POINT('',(-13.5,0.,-13.));
#32786=CARTESIAN_POINT('Ctrl Pts',(-13.5,1.68454855146387E-14,-13.));
#32787=CARTESIAN_POINT('Ctrl Pts',(-13.5,3.61731409783201,-13.));
#32788=CARTESIAN_POINT('Ctrl Pts',(-13.5,7.79422863408941,-11.7942286340514));
#32789=CARTESIAN_POINT('Ctrl Pts',(-13.5,-7.7942286340894,-11.7942286340514));
#32790=CARTESIAN_POINT('Ctrl Pts',(-13.5,-3.61731409783199,-13.));
#32791=CARTESIAN_POINT('Ctrl Pts',(-13.5,1.68454855146387E-14,-13.));
#32792=CARTESIAN_POINT('Origin',(-1.73472347597681E-15,15.5884572681199,
0.));
#32793=CARTESIAN_POINT('Origin',(0.,0.,0.));
#32794=CARTESIAN_POINT('Origin',(0.,0.,0.));
#32795=CARTESIAN_POINT('Origin',(0.,0.,0.));
#32796=CARTESIAN_POINT('Origin',(0.,0.,0.));
#32797=CARTESIAN_POINT('Origin',(0.,0.,0.));
#32798=CARTESIAN_POINT('Origin',(0.,0.,0.));
#32799=CARTESIAN_POINT('Origin',(-1.73472347597681E-15,15.5884572681199,
-13.));
#32800=CARTESIAN_POINT('Origin',(0.,0.,-13.));
#32801=CARTESIAN_POINT('Origin',(0.,0.,-13.));
#32802=CARTESIAN_POINT('Origin',(0.,0.,-13.));
#32803=CARTESIAN_POINT('Origin',(0.,0.,-13.));
#32804=CARTESIAN_POINT('Origin',(0.,0.,-13.));
#32805=CARTESIAN_POINT('Origin',(0.,0.,-13.));
#32806=CARTESIAN_POINT('Origin',(0.,0.,-13.));
#32807=CARTESIAN_POINT('Origin',(0.,0.,-13.));
#32808=CARTESIAN_POINT('Origin',(0.,0.,-13.));
#32809=CARTESIAN_POINT('Origin',(0.,0.,-13.));
#32810=CARTESIAN_POINT('Origin',(0.,0.,-13.));
#32811=CARTESIAN_POINT('Origin',(0.,0.,-13.));
#32812=CARTESIAN_POINT('Origin',(0.,0.,0.));
#32813=CARTESIAN_POINT('Origin',(0.,0.,0.));
#32814=CARTESIAN_POINT('Origin',(0.,0.,0.));
#32815=CARTESIAN_POINT('Origin',(0.,0.,0.));
#32816=CARTESIAN_POINT('Origin',(0.,0.,0.));
#32817=CARTESIAN_POINT('Origin',(0.,0.,0.));
#32885=UNCERTAINTY_MEASURE_WITH_UNIT(LENGTH_MEASURE(0.01),#32904,
'DISTANCE_ACCURACY_VALUE',
'Maximum model space distance between geometric entities at asserted c
onnectivities');
#32886=UNCERTAINTY_MEASURE_WITH_UNIT(LENGTH_MEASURE(0.01),#32904,
'DISTANCE_ACCURACY_VALUE',
'Maximum model space distance between geometric entities at asserted c
onnectivities');
#32902=(
GEOMETRIC_REPRESENTATION_CONTEXT(3)
GLOBAL_UNCERTAINTY_ASSIGNED_CONTEXT((#32885))
GLOBAL_UNIT_ASSIGNED_CONTEXT((#32904,#32906,#32907))
REPRESENTATION_CONTEXT('','3D')
);
#32903=(
GEOMETRIC_REPRESENTATION_CONTEXT(3)
GLOBAL_UNCERTAINTY_ASSIGNED_CONTEXT((#32886))
GLOBAL_UNIT_ASSIGNED_CONTEXT((#32904,#32906,#32907))
REPRESENTATION_CONTEXT('','3D')
);
#32904=(
LENGTH_UNIT()
NAMED_UNIT(*)
SI_UNIT(.MILLI.,.METRE.)
);
#32906=(
NAMED_UNIT(*)
PLANE_ANGLE_UNIT()
SI_UNIT($,.RADIAN.)
);
#32907=(
NAMED_UNIT(*)
SI_UNIT($,.STERADIAN.)
SOLID_ANGLE_UNIT()
);
#32923=SHAPE_DEFINITION_REPRESENTATION(#32959,#33027);
#32959=PRODUCT_DEFINITION_SHAPE('',$,#33044);
#33027=SHAPE_REPRESENTATION('',(#17061),#32902);
#33028=PRODUCT_DEFINITION_CONTEXT('part definition',#33078,'design');
#33044=PRODUCT_DEFINITION('High Strength Hex Nut DIN 6915 M16',
'High Strength Hex Nut DIN 6915 M16',#33060,#33028);
#33060=PRODUCT_DEFINITION_FORMATION('',$,#33095);
#33078=APPLICATION_CONTEXT(
'Core Data for Automotive Mechanical Design Process');
#33079=PRODUCT_CONTEXT('part definition',#33078,'mechanical');
#33095=PRODUCT('High Strength Hex Nut DIN 6915 M16',
'High Strength Hex Nut DIN 6915 M16',$,(#33079));
#33099=PRESENTATION_STYLE_ASSIGNMENT((#33105));
#33105=SURFACE_STYLE_USAGE(.BOTH.,#33111);
#33111=SURFACE_SIDE_STYLE('',(#33117));
#33117=SURFACE_STYLE_FILL_AREA(#33123);
#33123=FILL_AREA_STYLE('Opaque(31,36,43)',(#33129));
#33129=FILL_AREA_STYLE_COLOUR('Opaque(31,36,43)',#33135);
#33135=COLOUR_RGB('Opaque(31,36,43)',0.12156862745098,0.141176470588235,
0.168627450980392);
ENDSEC;
END-ISO-10303-21;
